ISO-10303-21;
HEADER;
FILE_DESCRIPTION (('STEP AP214'),
    '1' );
FILE_NAME ('Part2.step',
    '2026-10-09T16:01:55',
    ( '' ),
    ( '' ),
    'SwSTEP 2.0',
    'SolidWorks 2024',
    '' );
FILE_SCHEMA (( 'AUTOMOTIVE_DESIGN' ));
ENDSEC;

DATA;
#111=EDGE_CURVE ( 'NONE', #61998, #6695, #11268, .T. ) ;
#444=EDGE_CURVE ( 'NONE', #43479, #36887, #64517, .T. ) ;
#615=( GEOMETRIC_REPRESENTATION_CONTEXT ( 3 ) GLOBAL_UNCERTAINTY_ASSIGNED_CONTEXT ( ( #42268 ) ) GLOBAL_UNIT_ASSIGNED_CONTEXT ( ( #31322, #48608, #68779 ) ) REPRESENTATION_CONTEXT ( 'NONE', 'WORKASPACE' ) );
#883=PRODUCT_DEFINITION_FORMATION_WITH_SPECIFIED_SOURCE ( 'ANY', '', #35679, .NOT_KNOWN. ) ;
#1024=CARTESIAN_POINT ( 'NONE',  ( 52.83090410532631864, 61.65740854044500452, 0.000000000000000000 ) ) ;
#1202=DIRECTION ( 'NONE',  ( 1.000000000000000000, -0.000000000000000000, -0.000000000000000000 ) ) ;
#1479=EDGE_LOOP ( 'NONE', ( #65688, #31155, #2228, #38780 ) ) ;
#1536=CARTESIAN_POINT ( 'NONE',  ( 52.83090410532631864, 5.657408540445001854, 0.000000000000000000 ) ) ;
#1575=DIRECTION ( 'NONE',  ( -1.000000000000000000, 0.000000000000000000, 0.000000000000000000 ) ) ;
#1761=DIRECTION ( 'NONE',  ( -0.000000000000000000, 1.000000000000000000, 0.000000000000000000 ) ) ;
#1892=ADVANCED_FACE ( 'NONE', ( #11878 ), #54694, .F. ) ;
#2228=ORIENTED_EDGE ( 'NONE', *, *, #52293, .F. ) ;
#2382=VERTEX_POINT ( 'NONE', #68622 ) ;
#2447=DIRECTION ( 'NONE',  ( 0.000000000000000000, 1.000000000000000000, 0.000000000000000000 ) ) ;
#2607=LINE ( 'NONE', #60952, #2910 ) ;
#2625=FACE_OUTER_BOUND ( 'NONE', #43992, .T. ) ;
#2648=FACE_OUTER_BOUND ( 'NONE', #18794, .T. ) ;
#2769=PRODUCT_CONTEXT ( 'NONE', #27335, 'mechanical' ) ;
#2910=VECTOR ( 'NONE', #6862, 1000.000000000000000 ) ;
#3196=ORIENTED_EDGE ( 'NONE', *, *, #111, .F. ) ;
#3225=VECTOR ( 'NONE', #41858, 1000.000000000000000 ) ;
#3690=CARTESIAN_POINT ( 'NONE',  ( 105.8309041053263257, 61.65740854044500452, 2.000000000000000000 ) ) ;
#4050=DIRECTION ( 'NONE',  ( 0.000000000000000000, 0.000000000000000000, 1.000000000000000000 ) ) ;
#4279=VERTEX_POINT ( 'NONE', #12567 ) ;
#4659=ORIENTED_EDGE ( 'NONE', *, *, #40983, .F. ) ;
#5013=CARTESIAN_POINT ( 'NONE',  ( 105.8309041053263257, 3.657408540445008960, 2.000000000000000000 ) ) ;
#5470=DIRECTION ( 'NONE',  ( 0.000000000000000000, -1.000000000000000000, 0.000000000000000000 ) ) ;
#5516=VECTOR ( 'NONE', #32137, 1000.000000000000000 ) ;
#5531=LINE ( 'NONE', #5879, #47299 ) ;
#5879=CARTESIAN_POINT ( 'NONE',  ( 105.8309041053263257, 63.65740854044500452, 10.00000000000000000 ) ) ;
#5961=DIRECTION ( 'NONE',  ( 1.000000000000000000, -0.000000000000000000, -0.000000000000000000 ) ) ;
#6553=ORIENTED_EDGE ( 'NONE', *, *, #42173, .T. ) ;
#6695=VERTEX_POINT ( 'NONE', #18250 ) ;
#6862=DIRECTION ( 'NONE',  ( -1.000000000000000000, -1.301042606982605321E-16, -0.000000000000000000 ) ) ;
#6886=ORIENTED_EDGE ( 'NONE', *, *, #32454, .T. ) ;
#6990=CARTESIAN_POINT ( 'NONE',  ( 50.83090410532631864, 63.65740854044500452, 2.000000000000000000 ) ) ;
#7609=ADVANCED_FACE ( 'NONE', ( #36808 ), #52364, .T. ) ;
#7743=LINE ( 'NONE', #62187, #42248 ) ;
#8299=CARTESIAN_POINT ( 'NONE',  ( 105.8309041053263257, 5.657408540445008960, 2.000000000000000000 ) ) ;
#8659=CARTESIAN_POINT ( 'NONE',  ( 50.83090410532631864, 3.657408540445007628, 10.00000000000000000 ) ) ;
#9075=CARTESIAN_POINT ( 'NONE',  ( 105.8309041053263257, 63.65740854044500452, 10.00000000000000000 ) ) ;
#9400=ORIENTED_EDGE ( 'NONE', *, *, #40983, .T. ) ;
#9624=LINE ( 'NONE', #31199, #61656 ) ;
#9888=CARTESIAN_POINT ( 'NONE',  ( 105.8309041053263257, 5.657408540445008960, 0.000000000000000000 ) ) ;
#9893=LINE ( 'NONE', #31808, #61034 ) ;
#10414=FACE_OUTER_BOUND ( 'NONE', #15786, .T. ) ;
#11111=CARTESIAN_POINT ( 'NONE',  ( 0.000000000000000000, 61.65740854044500452, 0.000000000000000000 ) ) ;
#11268=LINE ( 'NONE', #58685, #67928 ) ;
#11430=EDGE_CURVE ( 'NONE', #2382, #18569, #7743, .T. ) ;
#11534=DIRECTION ( 'NONE',  ( -1.000000000000000000, -1.301042606982605321E-16, 0.000000000000000000 ) ) ;
#11878=FACE_OUTER_BOUND ( 'NONE', #61935, .T. ) ;
#12567=CARTESIAN_POINT ( 'NONE',  ( 52.83090410532631864, 5.657408540445001854, 0.000000000000000000 ) ) ;
#12929=ORIENTED_EDGE ( 'NONE', *, *, #33725, .F. ) ;
#13497=EDGE_CURVE ( 'NONE', #47507, #36887, #9624, .T. ) ;
#13669=VERTEX_POINT ( 'NONE', #5013 ) ;
#13801=CARTESIAN_POINT ( 'NONE',  ( 50.83090410532631864, 63.65740854044500452, 10.00000000000000000 ) ) ;
#14044=( BOUNDED_CURVE ( )  B_SPLINE_CURVE ( 3, ( #48958, #43649, #60592, #1536 ),
 .UNSPECIFIED., .F., .F. ) 
 B_SPLINE_CURVE_WITH_KNOTS ( ( 4, 4 ),
 ( 0.000000000000000000, 1.570796326794896558 ),
 .UNSPECIFIED. ) 
 CURVE ( )  GEOMETRIC_REPRESENTATION_ITEM ( )  RATIONAL_B_SPLINE_CURVE ( ( 1.000000000000000000, 0.8047378541243649375, 0.8047378541243649375, 1.000000000000000000 ) ) 
 REPRESENTATION_ITEM ( '' )  );
#14183=SHAPE_REPRESENTATION ( 'Part2', ( #45918 ), #65174 ) ;
#14210=LINE ( 'NONE', #46382, #5516 ) ;
#14308=FACE_OUTER_BOUND ( 'NONE', #19177, .T. ) ;
#15035=SURFACE_SIDE_STYLE ('',( #53569 ) ) ;
#15319=EDGE_CURVE ( 'NONE', #4279, #43479, #35312, .T. ) ;
#15701=ORIENTED_EDGE ( 'NONE', *, *, #13497, .F. ) ;
#15732=DIRECTION ( 'NONE',  ( -1.000000000000000000, 0.000000000000000000, 0.000000000000000000 ) ) ;
#15786=EDGE_LOOP ( 'NONE', ( #33866, #6886, #47258, #54633 ) ) ;
#16143=ADVANCED_FACE ( 'NONE', ( #22818 ), #44366, .F. ) ;
#16359=COLOUR_RGB ( '', 0.09019608, 0.27058824, 0.51372549) ;
#16647=CARTESIAN_POINT ( 'NONE',  ( 50.83090410532631864, 63.65740854044500452, 10.00000000000000000 ) ) ;
#17238=DIRECTION ( 'NONE',  ( 1.000000000000000000, 0.000000000000000000, -0.000000000000000000 ) ) ;
#17256=ORIENTED_EDGE ( 'NONE', *, *, #33725, .T. ) ;
#17620=ADVANCED_FACE ( 'NONE', ( #10414 ), #65544, .F. ) ;
#18250=CARTESIAN_POINT ( 'NONE',  ( 50.83090410532631864, 3.657408540445007628, 2.000000000000000000 ) ) ;
#18569=VERTEX_POINT ( 'NONE', #56064 ) ;
#18793=EDGE_LOOP ( 'NONE', ( #15701, #65307, #38834, #24144 ) ) ;
#18794=EDGE_LOOP ( 'NONE', ( #6553, #49629, #3196, #4659 ) ) ;
#18801=VECTOR ( 'NONE', #1761, 1000.000000000000000 ) ;
#18897=LINE ( 'NONE', #35490, #3225 ) ;
#19177=EDGE_LOOP ( 'NONE', ( #20159, #58074, #33055, #23288 ) ) ;
#19482=AXIS2_PLACEMENT_3D ( 'NONE', #42733, #65352, #17238 ) ;
#20159=ORIENTED_EDGE ( 'NONE', *, *, #30517, .F. ) ;
#20876=CARTESIAN_POINT ( 'NONE',  ( 52.83090410532631864, 3.657408540445007628, 2.000000000000000000 ) ) ;
#21647=PRODUCT_DEFINITION_SHAPE ( 'NONE', 'NONE',  #52984 ) ;
#21731=FILL_AREA_STYLE ('',( #37654 ) ) ;
#22306=AXIS2_PLACEMENT_3D ( 'NONE', #40738, #45679, #62294 ) ;
#22775=CARTESIAN_POINT ( 'NONE',  ( 0.000000000000000000, 0.000000000000000000, 0.000000000000000000 ) ) ;
#22818=FACE_OUTER_BOUND ( 'NONE', #18793, .T. ) ;
#23142=DIRECTION ( 'NONE',  ( 0.000000000000000000, 0.000000000000000000, 1.000000000000000000 ) ) ;
#23288=ORIENTED_EDGE ( 'NONE', *, *, #32454, .F. ) ;
#23479=ORIENTED_EDGE ( 'NONE', *, *, #11430, .F. ) ;
#24144=ORIENTED_EDGE ( 'NONE', *, *, #444, .T. ) ;
#24227=DIRECTION ( 'NONE',  ( 1.000000000000000000, 0.000000000000000000, 0.000000000000000000 ) ) ;
#24887=CARTESIAN_POINT ( 'NONE',  ( 50.83090410532631864, 3.657408540445007628, 10.00000000000000000 ) ) ;
#25911=ORIENTED_EDGE ( 'NONE', *, *, #52293, .T. ) ;
#26390=DIRECTION ( 'NONE',  ( 1.000000000000000000, 1.301042606982605321E-16, 0.000000000000000000 ) ) ;
#27092=DIRECTION ( 'NONE',  ( -1.000000000000000000, 0.000000000000000000, 0.000000000000000000 ) ) ;
#27107=EDGE_CURVE ( 'NONE', #47507, #4279, #2607, .T. ) ;
#27335=APPLICATION_CONTEXT ( 'automotive_design' ) ;
#29306=EDGE_LOOP ( 'NONE', ( #25911, #38029, #12929, #35469 ) ) ;
#29580=CIRCLE ( 'NONE', #42018, 2.000000000000000000 ) ;
#29876=CIRCLE ( 'NONE', #46836, 2.000000000000000000 ) ;
#29877=DIRECTION ( 'NONE',  ( 1.000000000000000000, 1.301042606982605321E-16, 0.000000000000000000 ) ) ;
#29981=CARTESIAN_POINT ( 'NONE',  ( 105.8309041053263257, 5.657408540445008960, 2.000000000000000000 ) ) ;
#30016=ORIENTED_EDGE ( 'NONE', *, *, #55335, .T. ) ;
#30124=LINE ( 'NONE', #51705, #62324 ) ;
#30517=EDGE_CURVE ( 'NONE', #36887, #60315, #29580, .T. ) ;
#30725=ORIENTED_EDGE ( 'NONE', *, *, #13497, .T. ) ;
#31155=ORIENTED_EDGE ( 'NONE', *, *, #15319, .F. ) ;
#31199=CARTESIAN_POINT ( 'NONE',  ( 105.8309041053263257, 3.657408540445008960, 0.000000000000000000 ) ) ;
#31322=( LENGTH_UNIT ( ) NAMED_UNIT ( * ) SI_UNIT ( .MILLI., .METRE. ) );
#31808=CARTESIAN_POINT ( 'NONE',  ( 50.83090410532631864, 3.657408540445007628, 10.00000000000000000 ) ) ;
#31821=DIRECTION ( 'NONE',  ( -0.000000000000000000, -0.000000000000000000, -1.000000000000000000 ) ) ;
#32000=CARTESIAN_POINT ( 'NONE',  ( 105.8309041053263257, 63.65740854044500452, 2.000000000000000000 ) ) ;
#32137=DIRECTION ( 'NONE',  ( 1.000000000000000000, 1.301042606982605321E-16, -0.000000000000000000 ) ) ;
#32355=DIRECTION ( 'NONE',  ( 1.000000000000000000, 0.000000000000000000, 0.000000000000000000 ) ) ;
#32454=EDGE_CURVE ( 'NONE', #60315, #35394, #47216, .T. ) ;
#33055=ORIENTED_EDGE ( 'NONE', *, *, #65699, .F. ) ;
#33725=EDGE_CURVE ( 'NONE', #13669, #47507, #29876, .T. ) ;
#33866=ORIENTED_EDGE ( 'NONE', *, *, #46620, .T. ) ;
#34014=CARTESIAN_POINT ( 'NONE',  ( 52.83090410532631864, 61.65740854044500452, 0.000000000000000000 ) ) ;
#34268=CARTESIAN_POINT ( 'NONE',  ( 52.83090410532631864, 0.000000000000000000, 0.000000000000000000 ) ) ;
#34485=CARTESIAN_POINT ( 'NONE',  ( 105.8309041053263257, 3.657408540445008960, 10.00000000000000000 ) ) ;
#35064=DIRECTION ( 'NONE',  ( -0.000000000000000000, -0.000000000000000000, -1.000000000000000000 ) ) ;
#35169=CYLINDRICAL_SURFACE ( 'NONE', #39896, 2.000000000000000000 ) ;
#35275=SHAPE_DEFINITION_REPRESENTATION ( #21647, #14183 ) ;
#35312=LINE ( 'NONE', #34268, #18801 ) ;
#35394=VERTEX_POINT ( 'NONE', #54804 ) ;
#35469=ORIENTED_EDGE ( 'NONE', *, *, #46609, .F. ) ;
#35490=CARTESIAN_POINT ( 'NONE',  ( 50.83090410532631864, 3.657408540445007628, 2.000000000000000000 ) ) ;
#35679=PRODUCT ( 'Part2', 'Part2', '', ( #2769 ) ) ;
#35989=DIRECTION ( 'NONE',  ( 0.000000000000000000, 0.000000000000000000, 1.000000000000000000 ) ) ;
#36150=( BOUNDED_CURVE ( )  B_SPLINE_CURVE ( 3, ( #6990, #44818, #65711, #1024 ),
 .UNSPECIFIED., .F., .F. ) 
 B_SPLINE_CURVE_WITH_KNOTS ( ( 4, 4 ),
 ( 3.141592653589793116, 4.712388980384689674 ),
 .UNSPECIFIED. ) 
 CURVE ( )  GEOMETRIC_REPRESENTATION_ITEM ( )  RATIONAL_B_SPLINE_CURVE ( ( 1.000000000000000000, 0.8047378541243649375, 0.8047378541243649375, 1.000000000000000000 ) ) 
 REPRESENTATION_ITEM ( '' )  );
#36808=FACE_OUTER_BOUND ( 'NONE', #1479, .T. ) ;
#36887=VERTEX_POINT ( 'NONE', #68295 ) ;
#37654=FILL_AREA_STYLE_COLOUR ( '', #16359 ) ;
#38029=ORIENTED_EDGE ( 'NONE', *, *, #27107, .F. ) ;
#38664=ADVANCED_FACE ( 'NONE', ( #2625 ), #50016, .F. ) ;
#38780=ORIENTED_EDGE ( 'NONE', *, *, #38816, .F. ) ;
#38816=EDGE_CURVE ( 'NONE', #35394, #6695, #18897, .T. ) ;
#38834=ORIENTED_EDGE ( 'NONE', *, *, #15319, .T. ) ;
#39479=APPLICATION_CONTEXT ( 'automotive_design' ) ;
#39896=AXIS2_PLACEMENT_3D ( 'NONE', #8299, #29877, #40835 ) ;
#40738=CARTESIAN_POINT ( 'NONE',  ( 0.000000000000000000, 0.000000000000000000, 0.000000000000000000 ) ) ;
#40835=DIRECTION ( 'NONE',  ( 0.000000000000000000, 1.000000000000000000, 0.000000000000000000 ) ) ;
#40983=EDGE_CURVE ( 'NONE', #68953, #61998, #9893, .T. ) ;
#41546=ORIENTED_EDGE ( 'NONE', *, *, #47934, .T. ) ;
#41777=ADVANCED_FACE ( 'NONE', ( #2648 ), #51089, .F. ) ;
#41858=DIRECTION ( 'NONE',  ( 0.000000000000000000, -1.000000000000000000, -0.000000000000000000 ) ) ;
#42018=AXIS2_PLACEMENT_3D ( 'NONE', #66030, #5961, #54748 ) ;
#42173=EDGE_CURVE ( 'NONE', #68953, #35394, #54814, .T. ) ;
#42245=PRESENTATION_STYLE_ASSIGNMENT (( #52520 ) ) ;
#42248=VECTOR ( 'NONE', #2447, 1000.000000000000000 ) ;
#42268=UNCERTAINTY_MEASURE_WITH_UNIT (LENGTH_MEASURE( 1.000000000000000082E-05 ), #31322, 'distance_accuracy_value', 'NONE');
#42616=ORIENTED_EDGE ( 'NONE', *, *, #111, .T. ) ;
#42733=CARTESIAN_POINT ( 'NONE',  ( 0.000000000000000000, 0.000000000000000000, 10.00000000000000000 ) ) ;
#43479=VERTEX_POINT ( 'NONE', #34014 ) ;
#43586=ADVANCED_BREP_SHAPE_REPRESENTATION ( '', ( #67347, #45918 ), #65174 ) ;
#43649=CARTESIAN_POINT ( 'NONE',  ( 50.83090410532631864, 3.657408540445001854, 0.8284271247461899579 ) ) ;
#43992=EDGE_LOOP ( 'NONE', ( #30016, #17256, #30725, #54047, #65579, #23479 ) ) ;
#44200=ORIENTED_EDGE ( 'NONE', *, *, #11430, .T. ) ;
#44366=PLANE ( 'NONE',  #22306 ) ;
#44818=CARTESIAN_POINT ( 'NONE',  ( 50.83090410532631864, 63.65740854044501162, 0.8284271247461908461 ) ) ;
#45026=( LENGTH_UNIT ( ) NAMED_UNIT ( * ) SI_UNIT ( .MILLI., .METRE. ) );
#45679=DIRECTION ( 'NONE',  ( 0.000000000000000000, -0.000000000000000000, 1.000000000000000000 ) ) ;
#45918=AXIS2_PLACEMENT_3D ( 'NONE', #22775, #53934, #32355 ) ;
#46081=( NAMED_UNIT ( * ) PLANE_ANGLE_UNIT ( ) SI_UNIT ( $, .RADIAN. ) );
#46244=AXIS2_PLACEMENT_3D ( 'NONE', #20876, #68971, #47058 ) ;
#46382=CARTESIAN_POINT ( 'NONE',  ( 105.8309041053263257, 3.657408540445008960, 10.00000000000000000 ) ) ;
#46609=EDGE_CURVE ( 'NONE', #6695, #13669, #68479, .T. ) ;
#46620=EDGE_CURVE ( 'NONE', #18569, #60315, #57506, .T. ) ;
#46836=AXIS2_PLACEMENT_3D ( 'NONE', #29981, #51558, #35989 ) ;
#47058=DIRECTION ( 'NONE',  ( 0.000000000000000000, 0.000000000000000000, -1.000000000000000000 ) ) ;
#47216=LINE ( 'NONE', #32000, #53105 ) ;
#47258=ORIENTED_EDGE ( 'NONE', *, *, #42173, .F. ) ;
#47299=VECTOR ( 'NONE', #27092, 1000.000000000000000 ) ;
#47474=EDGE_CURVE ( 'NONE', #61998, #2382, #14210, .T. ) ;
#47483=AXIS2_PLACEMENT_3D ( 'NONE', #8659, #24227, #68059 ) ;
#47507=VERTEX_POINT ( 'NONE', #9888 ) ;
#47708=DIRECTION ( 'NONE',  ( -0.000000000000000000, -1.000000000000000000, -0.000000000000000000 ) ) ;
#47934=EDGE_CURVE ( 'NONE', #18569, #68953, #5531, .T. ) ;
#48317=VECTOR ( 'NONE', #26390, 1000.000000000000000 ) ;
#48608=( NAMED_UNIT ( * ) PLANE_ANGLE_UNIT ( ) SI_UNIT ( $, .RADIAN. ) );
#48958=CARTESIAN_POINT ( 'NONE',  ( 50.83090410532631864, 3.657408540445007628, 2.000000000000000000 ) ) ;
#49551=ORIENTED_EDGE ( 'NONE', *, *, #46609, .T. ) ;
#49629=ORIENTED_EDGE ( 'NONE', *, *, #38816, .T. ) ;
#50016=PLANE ( 'NONE',  #68750 ) ;
#50524=VECTOR ( 'NONE', #69522, 1000.000000000000000 ) ;
#50712=CARTESIAN_POINT ( 'NONE',  ( 105.8309041053263257, 3.657408540445008960, 10.00000000000000000 ) ) ;
#51089=PLANE ( 'NONE',  #47483 ) ;
#51558=DIRECTION ( 'NONE',  ( 1.000000000000000000, -0.000000000000000000, -0.000000000000000000 ) ) ;
#51705=CARTESIAN_POINT ( 'NONE',  ( 105.8309041053263257, 3.657408540445008960, 10.00000000000000000 ) ) ;
#52293=EDGE_CURVE ( 'NONE', #6695, #4279, #14044, .T. ) ;
#52364=CYLINDRICAL_SURFACE ( 'NONE', #46244, 2.000000000000000000 ) ;
#52458=ORIENTED_EDGE ( 'NONE', *, *, #47474, .T. ) ;
#52486=DIRECTION ( 'NONE',  ( -1.000000000000000000, 0.000000000000000000, 0.000000000000000000 ) ) ;
#52520=SURFACE_STYLE_USAGE ( .BOTH. , #15035 ) ;
#52779=DIRECTION ( 'NONE',  ( 0.000000000000000000, 1.000000000000000000, 0.000000000000000000 ) ) ;
#52984=PRODUCT_DEFINITION ( 'UNKNOWN', '', #883, #60760 ) ;
#53105=VECTOR ( 'NONE', #15732, 1000.000000000000000 ) ;
#53208=VECTOR ( 'NONE', #65760, 1000.000000000000000 ) ;
#53569=SURFACE_STYLE_FILL_AREA ( #21731 ) ;
#53650=AXIS2_PLACEMENT_3D ( 'NONE', #69459, #5470, #58521 ) ;
#53934=DIRECTION ( 'NONE',  ( 0.000000000000000000, 0.000000000000000000, 1.000000000000000000 ) ) ;
#54047=ORIENTED_EDGE ( 'NONE', *, *, #30517, .T. ) ;
#54364=AXIS2_PLACEMENT_3D ( 'NONE', #34485, #66338, #11534 ) ;
#54396=PLANE ( 'NONE',  #19482 ) ;
#54633=ORIENTED_EDGE ( 'NONE', *, *, #47934, .F. ) ;
#54694=PLANE ( 'NONE',  #54364 ) ;
#54748=DIRECTION ( 'NONE',  ( 0.000000000000000000, 0.000000000000000000, 1.000000000000000000 ) ) ;
#54804=CARTESIAN_POINT ( 'NONE',  ( 50.83090410532631864, 63.65740854044500452, 2.000000000000000000 ) ) ;
#54814=LINE ( 'NONE', #16647, #53208 ) ;
#54945=ADVANCED_FACE ( 'NONE', ( #14308 ), #57430, .T. ) ;
#55335=EDGE_CURVE ( 'NONE', #2382, #13669, #30124, .T. ) ;
#56064=CARTESIAN_POINT ( 'NONE',  ( 105.8309041053263257, 63.65740854044500452, 10.00000000000000000 ) ) ;
#57026=STYLED_ITEM ( 'NONE', ( #42245 ), #67347 ) ;
#57430=CYLINDRICAL_SURFACE ( 'NONE', #62274, 2.000000000000000000 ) ;
#57506=LINE ( 'NONE', #9075, #50524 ) ;
#57688=VECTOR ( 'NONE', #1202, 1000.000000000000000 ) ;
#58074=ORIENTED_EDGE ( 'NONE', *, *, #444, .F. ) ;
#58104=CARTESIAN_POINT ( 'NONE',  ( 105.8309041053263257, 63.65740854044500452, 2.000000000000000000 ) ) ;
#58521=DIRECTION ( 'NONE',  ( 0.000000000000000000, -0.000000000000000000, -1.000000000000000000 ) ) ;
#58577=CARTESIAN_POINT ( 'NONE',  ( 105.8309041053263257, 3.657408540445008960, 2.000000000000000000 ) ) ;
#58685=CARTESIAN_POINT ( 'NONE',  ( 50.83090410532631864, 3.657408540445007628, 10.00000000000000000 ) ) ;
#59694=FACE_OUTER_BOUND ( 'NONE', #61981, .T. ) ;
#59927=UNCERTAINTY_MEASURE_WITH_UNIT (LENGTH_MEASURE( 1.000000000000000082E-05 ), #45026, 'distance_accuracy_value', 'NONE');
#60315=VERTEX_POINT ( 'NONE', #58104 ) ;
#60592=CARTESIAN_POINT ( 'NONE',  ( 51.65933123007250316, 4.485835665191191701, 7.173814858237198427E-17 ) ) ;
#60760=PRODUCT_DEFINITION_CONTEXT ( 'detailed design', #39479, 'design' ) ;
#60952=CARTESIAN_POINT ( 'NONE',  ( -7.360529556226213473E-16, 5.657408540444995637, 0.000000000000000000 ) ) ;
#61034=VECTOR ( 'NONE', #47708, 1000.000000000000000 ) ;
#61656=VECTOR ( 'NONE', #52779, 1000.000000000000000 ) ;
#61935=EDGE_LOOP ( 'NONE', ( #42616, #49551, #66604, #65657 ) ) ;
#61981=EDGE_LOOP ( 'NONE', ( #44200, #41546, #9400, #52458 ) ) ;
#61998=VERTEX_POINT ( 'NONE', #24887 ) ;
#62044=FACE_OUTER_BOUND ( 'NONE', #29306, .T. ) ;
#62187=CARTESIAN_POINT ( 'NONE',  ( 105.8309041053263257, 3.657408540445008960, 10.00000000000000000 ) ) ;
#62274=AXIS2_PLACEMENT_3D ( 'NONE', #3690, #52486, #4050 ) ;
#62294=DIRECTION ( 'NONE',  ( 1.000000000000000000, 0.000000000000000000, -0.000000000000000000 ) ) ;
#62324=VECTOR ( 'NONE', #35064, 1000.000000000000000 ) ;
#63445=CLOSED_SHELL ( 'NONE', ( #38664, #17620, #41777, #1892, #64362, #16143, #54945, #7609, #66224 ) ) ;
#64362=ADVANCED_FACE ( 'NONE', ( #59694 ), #54396, .T. ) ;
#64517=LINE ( 'NONE', #11111, #57688 ) ;
#65174=( GEOMETRIC_REPRESENTATION_CONTEXT ( 3 ) GLOBAL_UNCERTAINTY_ASSIGNED_CONTEXT ( ( #59927 ) ) GLOBAL_UNIT_ASSIGNED_CONTEXT ( ( #45026, #46081, #66600 ) ) REPRESENTATION_CONTEXT ( 'NONE', 'WORKASPACE' ) );
#65307=ORIENTED_EDGE ( 'NONE', *, *, #27107, .T. ) ;
#65352=DIRECTION ( 'NONE',  ( 0.000000000000000000, -0.000000000000000000, 1.000000000000000000 ) ) ;
#65544=PLANE ( 'NONE',  #53650 ) ;
#65579=ORIENTED_EDGE ( 'NONE', *, *, #46620, .F. ) ;
#65657=ORIENTED_EDGE ( 'NONE', *, *, #47474, .F. ) ;
#65688=ORIENTED_EDGE ( 'NONE', *, *, #65699, .T. ) ;
#65699=EDGE_CURVE ( 'NONE', #35394, #43479, #36150, .T. ) ;
#65711=CARTESIAN_POINT ( 'NONE',  ( 51.65933123007250316, 62.82898141569881290, 6.488953147413177264E-16 ) ) ;
#65760=DIRECTION ( 'NONE',  ( -0.000000000000000000, -0.000000000000000000, -1.000000000000000000 ) ) ;
#66030=CARTESIAN_POINT ( 'NONE',  ( 105.8309041053263257, 61.65740854044500452, 2.000000000000000000 ) ) ;
#66051=MECHANICAL_DESIGN_GEOMETRIC_PRESENTATION_REPRESENTATION('',(#57026),#615);
#66224=ADVANCED_FACE ( 'NONE', ( #62044 ), #35169, .T. ) ;
#66338=DIRECTION ( 'NONE',  ( -1.301042606982605321E-16, 1.000000000000000000, 0.000000000000000000 ) ) ;
#66600=( NAMED_UNIT ( * ) SI_UNIT ( $, .STERADIAN. ) SOLID_ANGLE_UNIT ( ) );
#66604=ORIENTED_EDGE ( 'NONE', *, *, #55335, .F. ) ;
#66942=SHAPE_REPRESENTATION_RELATIONSHIP ( 'NONE' , 'NONE' ,  #14183, #43586 ) ;
#67347=MANIFOLD_SOLID_BREP ( 'Fillet1', #63445 ) ;
#67928=VECTOR ( 'NONE', #31821, 1000.000000000000000 ) ;
#68059=DIRECTION ( 'NONE',  ( 0.000000000000000000, 0.000000000000000000, -1.000000000000000000 ) ) ;
#68295=CARTESIAN_POINT ( 'NONE',  ( 105.8309041053263257, 61.65740854044500452, 0.000000000000000000 ) ) ;
#68479=LINE ( 'NONE', #58577, #48317 ) ;
#68622=CARTESIAN_POINT ( 'NONE',  ( 105.8309041053263257, 3.657408540445008960, 10.00000000000000000 ) ) ;
#68750=AXIS2_PLACEMENT_3D ( 'NONE', #50712, #1575, #23142 ) ;
#68779=( NAMED_UNIT ( * ) SI_UNIT ( $, .STERADIAN. ) SOLID_ANGLE_UNIT ( ) );
#68953=VERTEX_POINT ( 'NONE', #13801 ) ;
#68971=DIRECTION ( 'NONE',  ( 0.000000000000000000, -1.000000000000000000, -0.000000000000000000 ) ) ;
#69459=CARTESIAN_POINT ( 'NONE',  ( 105.8309041053263257, 63.65740854044500452, 10.00000000000000000 ) ) ;
#69522=DIRECTION ( 'NONE',  ( -0.000000000000000000, -0.000000000000000000, -1.000000000000000000 ) ) ;
ENDSEC;
END-ISO-10303-21;
